ISO-10303-21;
HEADER;
/* Generated by software containing ST-Developer
 * from STEP Tools, Inc. (www.steptools.com) 
 */

FILE_DESCRIPTION(
/* description */ (''),
/* implementation_level */ '2;1');

FILE_NAME(
/* name */ 'Screw_Holder.step',
/* time_stamp */ '2026-10-19T01:17:59+06:00',
/* author */ (''),
/* organization */ (''),
/* preprocessor_version */ 'ST-DEVELOPER v20.2',
/* originating_system */ 'Autodesk Translation Framework v15.15.0.0',
/* authorisation */ '');

FILE_SCHEMA (('AUTOMOTIVE_DESIGN { 1 0 10303 214 3 1 1 }'));
ENDSEC;

DATA;
#10=MECHANICAL_DESIGN_GEOMETRIC_PRESENTATION_REPRESENTATION('',(#753),#48369);
#622=SHAPE_REPRESENTATION_RELATIONSHIP('SRR','None',#48422,#633);
#633=ADVANCED_BREP_SHAPE_REPRESENTATION('',(#779),#48367);
#727=FACE_BOUND('',#3350,.T.);
#728=FACE_BOUND('',#3352,.T.);
#753=STYLED_ITEM('',(#48524),#779);
#779=MANIFOLD_SOLID_BREP('Screw_Holder',#20132);
#1188=CYLINDRICAL_SURFACE('',#21830,17.5);
#2208=FACE_OUTER_BOUND('',#3344,.T.);
#2209=FACE_OUTER_BOUND('',#3345,.T.);
#2210=FACE_OUTER_BOUND('',#3346,.T.);
#2211=FACE_OUTER_BOUND('',#3347,.T.);
#2212=FACE_OUTER_BOUND('',#3348,.T.);
#2213=FACE_OUTER_BOUND('',#3349,.T.);
#2214=FACE_OUTER_BOUND('',#3351,.T.);
#3344=EDGE_LOOP('',(#18301,#18302,#18303,#18304));
#3345=EDGE_LOOP('',(#18305,#18306,#18307,#18308));
#3346=EDGE_LOOP('',(#18309,#18310,#18311,#18312));
#3347=EDGE_LOOP('',(#18313,#18314,#18315,#18316));
#3348=EDGE_LOOP('',(#18317,#18318,#18319,#18320));
#3349=EDGE_LOOP('',(#18321,#18322,#18323,#18324));
#3350=EDGE_LOOP('',(#18325));
#3351=EDGE_LOOP('',(#18326,#18327,#18328,#18329));
#3352=EDGE_LOOP('',(#18330));
#3955=CIRCLE('',#21831,17.5);
#3956=CIRCLE('',#21832,17.5);
#5795=LINE('',#48095,#7676);
#5796=LINE('',#48100,#7677);
#5797=LINE('',#48102,#7678);
#5798=LINE('',#48104,#7679);
#5799=LINE('',#48105,#7680);
#5800=LINE('',#48108,#7681);
#5801=LINE('',#48110,#7682);
#5802=LINE('',#48111,#7683);
#5803=LINE('',#48114,#7684);
#5804=LINE('',#48116,#7685);
#5805=LINE('',#48117,#7686);
#5806=LINE('',#48119,#7687);
#5807=LINE('',#48120,#7688);
#7676=VECTOR('',#26880,17.5);
#7677=VECTOR('',#26885,10.);
#7678=VECTOR('',#26886,10.);
#7679=VECTOR('',#26887,10.);
#7680=VECTOR('',#26888,10.);
#7681=VECTOR('',#26891,10.);
#7682=VECTOR('',#26892,10.);
#7683=VECTOR('',#26893,10.);
#7684=VECTOR('',#26896,10.);
#7685=VECTOR('',#26897,10.);
#7686=VECTOR('',#26898,10.);
#7687=VECTOR('',#26901,10.);
#7688=VECTOR('',#26902,10.);
#9631=VERTEX_POINT('',#48092);
#9632=VERTEX_POINT('',#48094);
#9633=VERTEX_POINT('',#48098);
#9634=VERTEX_POINT('',#48099);
#9635=VERTEX_POINT('',#48101);
#9636=VERTEX_POINT('',#48103);
#9637=VERTEX_POINT('',#48107);
#9638=VERTEX_POINT('',#48109);
#9639=VERTEX_POINT('',#48113);
#9640=VERTEX_POINT('',#48115);
#12534=EDGE_CURVE('',#9631,#9631,#3955,.T.);
#12535=EDGE_CURVE('',#9631,#9632,#5795,.T.);
#12536=EDGE_CURVE('',#9632,#9632,#3956,.T.);
#12537=EDGE_CURVE('',#9633,#9634,#5796,.T.);
#12538=EDGE_CURVE('',#9634,#9635,#5797,.T.);
#12539=EDGE_CURVE('',#9636,#9635,#5798,.T.);
#12540=EDGE_CURVE('',#9633,#9636,#5799,.T.);
#12541=EDGE_CURVE('',#9637,#9633,#5800,.T.);
#12542=EDGE_CURVE('',#9638,#9636,#5801,.T.);
#12543=EDGE_CURVE('',#9637,#9638,#5802,.T.);
#12544=EDGE_CURVE('',#9639,#9637,#5803,.T.);
#12545=EDGE_CURVE('',#9640,#9638,#5804,.T.);
#12546=EDGE_CURVE('',#9639,#9640,#5805,.T.);
#12547=EDGE_CURVE('',#9634,#9639,#5806,.T.);
#12548=EDGE_CURVE('',#9635,#9640,#5807,.T.);
#18301=ORIENTED_EDGE('',*,*,#12534,.F.);
#18302=ORIENTED_EDGE('',*,*,#12535,.T.);
#18303=ORIENTED_EDGE('',*,*,#12536,.F.);
#18304=ORIENTED_EDGE('',*,*,#12535,.F.);
#18305=ORIENTED_EDGE('',*,*,#12537,.T.);
#18306=ORIENTED_EDGE('',*,*,#12538,.T.);
#18307=ORIENTED_EDGE('',*,*,#12539,.F.);
#18308=ORIENTED_EDGE('',*,*,#12540,.F.);
#18309=ORIENTED_EDGE('',*,*,#12541,.T.);
#18310=ORIENTED_EDGE('',*,*,#12540,.T.);
#18311=ORIENTED_EDGE('',*,*,#12542,.F.);
#18312=ORIENTED_EDGE('',*,*,#12543,.F.);
#18313=ORIENTED_EDGE('',*,*,#12544,.T.);
#18314=ORIENTED_EDGE('',*,*,#12543,.T.);
#18315=ORIENTED_EDGE('',*,*,#12545,.F.);
#18316=ORIENTED_EDGE('',*,*,#12546,.F.);
#18317=ORIENTED_EDGE('',*,*,#12547,.T.);
#18318=ORIENTED_EDGE('',*,*,#12546,.T.);
#18319=ORIENTED_EDGE('',*,*,#12548,.F.);
#18320=ORIENTED_EDGE('',*,*,#12538,.F.);
#18321=ORIENTED_EDGE('',*,*,#12547,.F.);
#18322=ORIENTED_EDGE('',*,*,#12537,.F.);
#18323=ORIENTED_EDGE('',*,*,#12541,.F.);
#18324=ORIENTED_EDGE('',*,*,#12544,.F.);
#18325=ORIENTED_EDGE('',*,*,#12536,.T.);
#18326=ORIENTED_EDGE('',*,*,#12548,.T.);
#18327=ORIENTED_EDGE('',*,*,#12545,.T.);
#18328=ORIENTED_EDGE('',*,*,#12542,.T.);
#18329=ORIENTED_EDGE('',*,*,#12539,.T.);
#18330=ORIENTED_EDGE('',*,*,#12534,.T.);
#19040=PLANE('',#21833);
#19041=PLANE('',#21834);
#19042=PLANE('',#21835);
#19043=PLANE('',#21836);
#19044=PLANE('',#21837);
#19045=PLANE('',#21838);
#20065=ADVANCED_FACE('',(#2208),#1188,.F.);
#20066=ADVANCED_FACE('',(#2209),#19040,.T.);
#20067=ADVANCED_FACE('',(#2210),#19041,.T.);
#20068=ADVANCED_FACE('',(#2211),#19042,.T.);
#20069=ADVANCED_FACE('',(#2212),#19043,.T.);
#20070=ADVANCED_FACE('',(#2213,#727),#19044,.T.);
#20071=ADVANCED_FACE('',(#2214,#728),#19045,.F.);
#20132=CLOSED_SHELL('',(#20065,#20066,#20067,#20068,#20069,#20070,#20071));
#21829=AXIS2_PLACEMENT_3D('',#48090,#26874,#26875);
#21830=AXIS2_PLACEMENT_3D('',#48091,#26876,#26877);
#21831=AXIS2_PLACEMENT_3D('',#48093,#26878,#26879);
#21832=AXIS2_PLACEMENT_3D('',#48096,#26881,#26882);
#21833=AXIS2_PLACEMENT_3D('',#48097,#26883,#26884);
#21834=AXIS2_PLACEMENT_3D('',#48106,#26889,#26890);
#21835=AXIS2_PLACEMENT_3D('',#48112,#26894,#26895);
#21836=AXIS2_PLACEMENT_3D('',#48118,#26899,#26900);
#21837=AXIS2_PLACEMENT_3D('',#48121,#26903,#26904);
#21838=AXIS2_PLACEMENT_3D('',#48122,#26905,#26906);
#26874=DIRECTION('axis',(0.,0.,1.));
#26875=DIRECTION('refdir',(1.,0.,0.));
#26876=DIRECTION('center_axis',(0.,1.,0.));
#26877=DIRECTION('ref_axis',(-1.,0.,0.));
#26878=DIRECTION('center_axis',(0.,-1.,0.));
#26879=DIRECTION('ref_axis',(-1.,0.,0.));
#26880=DIRECTION('',(0.,-1.,0.));
#26881=DIRECTION('center_axis',(0.,1.,0.));
#26882=DIRECTION('ref_axis',(-1.,0.,0.));
#26883=DIRECTION('center_axis',(-1.,0.,0.));
#26884=DIRECTION('ref_axis',(0.,0.,1.));
#26885=DIRECTION('',(0.,0.,1.));
#26886=DIRECTION('',(0.,1.,0.));
#26887=DIRECTION('',(0.,0.,1.));
#26888=DIRECTION('',(0.,1.,0.));
#26889=DIRECTION('center_axis',(0.,0.,-1.));
#26890=DIRECTION('ref_axis',(-1.,0.,0.));
#26891=DIRECTION('',(-1.,0.,0.));
#26892=DIRECTION('',(-1.,0.,0.));
#26893=DIRECTION('',(0.,1.,0.));
#26894=DIRECTION('center_axis',(1.,0.,0.));
#26895=DIRECTION('ref_axis',(0.,0.,-1.));
#26896=DIRECTION('',(0.,0.,-1.));
#26897=DIRECTION('',(0.,0.,-1.));
#26898=DIRECTION('',(0.,1.,0.));
#26899=DIRECTION('center_axis',(0.,0.,1.));
#26900=DIRECTION('ref_axis',(1.,0.,0.));
#26901=DIRECTION('',(1.,0.,0.));
#26902=DIRECTION('',(1.,0.,0.));
#26903=DIRECTION('center_axis',(0.,-1.,0.));
#26904=DIRECTION('ref_axis',(-1.,0.,0.));
#26905=DIRECTION('center_axis',(0.,-1.,0.));
#26906=DIRECTION('ref_axis',(-1.,0.,0.));
#48090=CARTESIAN_POINT('',(0.,0.,0.));
#48091=CARTESIAN_POINT('Origin',(74.9879498948689,415.,53.0228109606356));
#48092=CARTESIAN_POINT('',(92.4879498948689,435.,53.0228109606356));
#48093=CARTESIAN_POINT('Origin',(74.9879498948689,435.,53.0228109606356));
#48094=CARTESIAN_POINT('',(92.4879498948689,415.,53.0228109606356));
#48095=CARTESIAN_POINT('',(92.4879498948689,415.,53.0228109606356));
#48096=CARTESIAN_POINT('Origin',(74.9879498948689,415.,53.0228109606356));
#48097=CARTESIAN_POINT('Origin',(37.9634359091503,415.,30.));
#48098=CARTESIAN_POINT('',(37.9634359091503,415.,30.));
#48099=CARTESIAN_POINT('',(37.9634359091503,415.,76.0456219212711));
#48100=CARTESIAN_POINT('',(37.9634359091503,415.,30.));
#48101=CARTESIAN_POINT('',(37.9634359091503,435.,76.0456219212711));
#48102=CARTESIAN_POINT('',(37.9634359091503,415.,76.0456219212711));
#48103=CARTESIAN_POINT('',(37.9634359091503,435.,30.));
#48104=CARTESIAN_POINT('',(37.9634359091503,435.,30.));
#48105=CARTESIAN_POINT('',(37.9634359091503,415.,30.));
#48106=CARTESIAN_POINT('Origin',(112.012463880588,415.,30.));
#48107=CARTESIAN_POINT('',(112.012463880588,415.,30.));
#48108=CARTESIAN_POINT('',(112.012463880588,415.,30.));
#48109=CARTESIAN_POINT('',(112.012463880588,435.,30.));
#48110=CARTESIAN_POINT('',(112.012463880588,435.,30.));
#48111=CARTESIAN_POINT('',(112.012463880588,415.,30.));
#48112=CARTESIAN_POINT('Origin',(112.012463880588,415.,76.0456219212711));
#48113=CARTESIAN_POINT('',(112.012463880588,415.,76.0456219212711));
#48114=CARTESIAN_POINT('',(112.012463880588,415.,76.0456219212711));
#48115=CARTESIAN_POINT('',(112.012463880588,435.,76.0456219212711));
#48116=CARTESIAN_POINT('',(112.012463880588,435.,76.0456219212711));
#48117=CARTESIAN_POINT('',(112.012463880588,415.,76.0456219212711));
#48118=CARTESIAN_POINT('Origin',(37.9634359091503,415.,76.0456219212711));
#48119=CARTESIAN_POINT('',(37.9634359091503,415.,76.0456219212711));
#48120=CARTESIAN_POINT('',(37.9634359091503,435.,76.0456219212711));
#48121=CARTESIAN_POINT('Origin',(74.9879498948689,415.,53.0228109606356));
#48122=CARTESIAN_POINT('Origin',(74.9879498948689,435.,53.0228109606356));
#48354=UNCERTAINTY_MEASURE_WITH_UNIT(LENGTH_MEASURE(0.01),#48370,
'DISTANCE_ACCURACY_VALUE',
'Maximum model space distance between geometric entities at asserted c
onnectivities');
#48356=UNCERTAINTY_MEASURE_WITH_UNIT(LENGTH_MEASURE(0.01),#48370,
'DISTANCE_ACCURACY_VALUE',
'Maximum model space distance between geometric entities at asserted c
onnectivities');
#48367=(
GEOMETRIC_REPRESENTATION_CONTEXT(3)
GLOBAL_UNCERTAINTY_ASSIGNED_CONTEXT((#48354))
GLOBAL_UNIT_ASSIGNED_CONTEXT((#48370,#48372,#48373))
REPRESENTATION_CONTEXT('','3D')
);
#48369=(
GEOMETRIC_REPRESENTATION_CONTEXT(3)
GLOBAL_UNCERTAINTY_ASSIGNED_CONTEXT((#48356))
GLOBAL_UNIT_ASSIGNED_CONTEXT((#48370,#48372,#48373))
REPRESENTATION_CONTEXT('','3D')
);
#48370=(
LENGTH_UNIT()
NAMED_UNIT(*)
SI_UNIT(.MILLI.,.METRE.)
);
#48372=(
NAMED_UNIT(*)
PLANE_ANGLE_UNIT()
SI_UNIT($,.RADIAN.)
);
#48373=(
NAMED_UNIT(*)
SI_UNIT($,.STERADIAN.)
SOLID_ANGLE_UNIT()
);
#48384=SHAPE_DEFINITION_REPRESENTATION(#48396,#48422);
#48396=PRODUCT_DEFINITION_SHAPE('',$,#48435);
#48422=SHAPE_REPRESENTATION('',(#21829),#48367);
#48424=PRODUCT_DEFINITION_CONTEXT('part definition',#48462,'design');
#48435=PRODUCT_DEFINITION('Screw_Holder','Screw_Holder',#48447,#48424);
#48447=PRODUCT_DEFINITION_FORMATION('',$,#48474);
#48462=APPLICATION_CONTEXT(
'Core Data for Automotive Mechanical Design Process');
#48463=PRODUCT_CONTEXT('part definition',#48462,'mechanical');
#48474=PRODUCT('Screw_Holder','Screw_Holder',$,(#48463));
#48518=COLOUR_RGB('Black',0.12,0.14,0.17);
#48519=FILL_AREA_STYLE_COLOUR('',#48518);
#48520=FILL_AREA_STYLE('',(#48519));
#48521=SURFACE_STYLE_FILL_AREA(#48520);
#48522=SURFACE_SIDE_STYLE('',(#48521));
#48523=SURFACE_STYLE_USAGE(.BOTH.,#48522);
#48524=PRESENTATION_STYLE_ASSIGNMENT((#48523));
ENDSEC;
END-ISO-10303-21;
